ISO-10303-21;
HEADER;
FILE_DESCRIPTION((''),'2;1');
FILE_NAME('Washer_1.step','2026-10-09T10:15:02-07:00',(''),(''),'','','');
FILE_SCHEMA (('AUTOMOTIVE_DESIGN { 1 0 10303 214 3 1 1 }'));
ENDSEC;
DATA;
#10=MECHANICAL_DESIGN_GEOMETRIC_PRESENTATION_REPRESENTATION('',(#85),#6779);
#65=SHAPE_REPRESENTATION_RELATIONSHIP('SRR','None',#6819,#75) ;
#75=ADVANCED_BREP_SHAPE_REPRESENTATION('',(#95),#6771) ;
#85=STYLED_ITEM('',(#6877),#95) ;
#95=MANIFOLD_SOLID_BREP('Body1',#3897) ;
#119=FACE_BOUND('',#758,.T.) ;
#120=FACE_BOUND('',#760,.T.) ;
#215=PLANE('',#4298) ;
#216=PLANE('',#4299) ;
#495=FACE_OUTER_BOUND('',#755,.T.) ;
#496=FACE_OUTER_BOUND('',#756,.T.) ;
#497=FACE_OUTER_BOUND('',#757,.T.) ;
#498=FACE_OUTER_BOUND('',#759,.T.) ;
#755=EDGE_LOOP('',(#3315,#3316,#3317,#3318)) ;
#756=EDGE_LOOP('',(#3319,#3320,#3321,#3322)) ;
#757=EDGE_LOOP('',(#3323)) ;
#758=EDGE_LOOP('',(#3324)) ;
#759=EDGE_LOOP('',(#3325)) ;
#760=EDGE_LOOP('',(#3326)) ;
#1115=LINE('',#6431,#1475) ;
#1116=LINE('',#6437,#1476) ;
#1475=VECTOR('',#5261,6.) ;
#1476=VECTOR('',#5268,3.2) ;
#1671=CIRCLE('',#4293,6.) ;
#1672=CIRCLE('',#4294,6.) ;
#1673=CIRCLE('',#4296,3.2) ;
#1674=CIRCLE('',#4297,3.2) ;
#1939=VERTEX_POINT('',#6428) ;
#1940=VERTEX_POINT('',#6430) ;
#1941=VERTEX_POINT('',#6434) ;
#1942=VERTEX_POINT('',#6436) ;
#2411=EDGE_CURVE('',#1939,#1939,#1671,.T.) ;
#2412=EDGE_CURVE('',#1939,#1940,#1115,.T.) ;
#2413=EDGE_CURVE('',#1940,#1940,#1672,.T.) ;
#2414=EDGE_CURVE('',#1941,#1941,#1673,.T.) ;
#2415=EDGE_CURVE('',#1941,#1942,#1116,.T.) ;
#2416=EDGE_CURVE('',#1942,#1942,#1674,.T.) ;
#3315=ORIENTED_EDGE('',*,*,#2411,.F.) ;
#3316=ORIENTED_EDGE('',*,*,#2412,.T.) ;
#3317=ORIENTED_EDGE('',*,*,#2413,.T.) ;
#3318=ORIENTED_EDGE('',*,*,#2412,.F.) ;
#3319=ORIENTED_EDGE('',*,*,#2414,.F.) ;
#3320=ORIENTED_EDGE('',*,*,#2415,.T.) ;
#3321=ORIENTED_EDGE('',*,*,#2416,.T.) ;
#3322=ORIENTED_EDGE('',*,*,#2415,.F.) ;
#3323=ORIENTED_EDGE('',*,*,#2413,.F.) ;
#3324=ORIENTED_EDGE('',*,*,#2414,.T.) ;
#3325=ORIENTED_EDGE('',*,*,#2411,.T.) ;
#3326=ORIENTED_EDGE('',*,*,#2416,.F.) ;
#3635=CYLINDRICAL_SURFACE('',#4292,6.) ;
#3636=CYLINDRICAL_SURFACE('',#4295,3.2) ;
#3819=ADVANCED_FACE('',(#495),#3635,.T.) ;
#3820=ADVANCED_FACE('',(#496),#3636,.F.) ;
#3821=ADVANCED_FACE('',(#497,#119),#215,.F.) ;
#3822=ADVANCED_FACE('',(#498,#120),#216,.T.) ;
#3897=CLOSED_SHELL('',(#3819,#3820,#3821,#3822)) ;
#4291=AXIS2_PLACEMENT_3D('',#6426,#5255,#5256) ;
#4292=AXIS2_PLACEMENT_3D('',#6427,#5257,#5258) ;
#4293=AXIS2_PLACEMENT_3D('',#6429,#5259,#5260) ;
#4294=AXIS2_PLACEMENT_3D('',#6432,#5262,#5263) ;
#4295=AXIS2_PLACEMENT_3D('',#6433,#5264,#5265) ;
#4296=AXIS2_PLACEMENT_3D('',#6435,#5266,#5267) ;
#4297=AXIS2_PLACEMENT_3D('',#6438,#5269,#5270) ;
#4298=AXIS2_PLACEMENT_3D('',#6439,#5271,#5272) ;
#4299=AXIS2_PLACEMENT_3D('',#6440,#5273,#5274) ;
#5255=DIRECTION('axis',(0.,0.,1.)) ;
#5256=DIRECTION('refdir',(1.,0.,0.)) ;
#5257=DIRECTION('center_axis',(0.,-1.,0.)) ;
#5258=DIRECTION('ref_axis',(1.,0.,0.)) ;
#5259=DIRECTION('center_axis',(0.,-1.,0.)) ;
#5260=DIRECTION('ref_axis',(0.,0.,1.)) ;
#5261=DIRECTION('',(0.,1.,0.)) ;
#5262=DIRECTION('center_axis',(0.,-1.,0.)) ;
#5263=DIRECTION('ref_axis',(0.,0.,1.)) ;
#5264=DIRECTION('center_axis',(0.,-1.,0.)) ;
#5265=DIRECTION('ref_axis',(1.,0.,0.)) ;
#5266=DIRECTION('center_axis',(0.,-1.,0.)) ;
#5267=DIRECTION('ref_axis',(0.,0.,1.)) ;
#5268=DIRECTION('',(0.,-1.,0.)) ;
#5269=DIRECTION('center_axis',(0.,-1.,0.)) ;
#5270=DIRECTION('ref_axis',(0.,0.,1.)) ;
#5271=DIRECTION('center_axis',(0.,-1.,0.)) ;
#5272=DIRECTION('ref_axis',(1.,0.,0.)) ;
#5273=DIRECTION('center_axis',(0.,-1.,0.)) ;
#5274=DIRECTION('ref_axis',(1.,0.,0.)) ;
#6426=CARTESIAN_POINT('',(0.,0.,0.)) ;
#6427=CARTESIAN_POINT('Origin',(-35.,-19.5,10.)) ;
#6428=CARTESIAN_POINT('',(-41.,-20.,10.)) ;
#6429=CARTESIAN_POINT('Origin',(-35.,-20.,10.)) ;
#6430=CARTESIAN_POINT('',(-41.,-19.,10.)) ;
#6431=CARTESIAN_POINT('',(-41.,-19.5,10.)) ;
#6432=CARTESIAN_POINT('Origin',(-35.,-19.,10.)) ;
#6433=CARTESIAN_POINT('Origin',(-35.,-19.5,10.)) ;
#6434=CARTESIAN_POINT('',(-38.2,-19.,10.)) ;
#6435=CARTESIAN_POINT('Origin',(-35.,-19.,10.)) ;
#6436=CARTESIAN_POINT('',(-38.2,-20.,10.)) ;
#6437=CARTESIAN_POINT('',(-38.2,-19.5,10.)) ;
#6438=CARTESIAN_POINT('Origin',(-35.,-20.,10.)) ;
#6439=CARTESIAN_POINT('Origin',(0.,-19.,0.)) ;
#6440=CARTESIAN_POINT('Origin',(0.,-20.,0.)) ;
#6759=UNCERTAINTY_MEASURE_WITH_UNIT(LENGTH_MEASURE(0.01),#6780,
'DISTANCE_ACCURACY_VALUE',
'Maximum model space distance between geometric entities at asserted c
onnectivities') ;
#6767=UNCERTAINTY_MEASURE_WITH_UNIT(LENGTH_MEASURE(0.01),#6780,
'DISTANCE_ACCURACY_VALUE',
'Maximum model space distance between geometric entities at asserted c
onnectivities') ;
#6771=(
GEOMETRIC_REPRESENTATION_CONTEXT(3)
GLOBAL_UNCERTAINTY_ASSIGNED_CONTEXT((#6759))
GLOBAL_UNIT_ASSIGNED_CONTEXT((#6780,#6782,#6783))
REPRESENTATION_CONTEXT('','3D')
) ;
#6779=(
GEOMETRIC_REPRESENTATION_CONTEXT(3)
GLOBAL_UNCERTAINTY_ASSIGNED_CONTEXT((#6767))
GLOBAL_UNIT_ASSIGNED_CONTEXT((#6780,#6782,#6783))
REPRESENTATION_CONTEXT('','3D')
) ;
#6780=(
LENGTH_UNIT()
NAMED_UNIT(*)
SI_UNIT(.MILLI.,.METRE.)
) ;
#6782=(
NAMED_UNIT(*)
PLANE_ANGLE_UNIT()
SI_UNIT($,.RADIAN.)
) ;
#6783=(
NAMED_UNIT(*)
SI_UNIT($,.STERADIAN.)
SOLID_ANGLE_UNIT()
) ;
#6787=SHAPE_DEFINITION_REPRESENTATION(#6798,#6819) ;
#6798=PRODUCT_DEFINITION_SHAPE('',$,#6831) ;
#6819=SHAPE_REPRESENTATION('',(#4291),#6771) ;
#6827=PRODUCT_DEFINITION_CONTEXT('part definition',#6862,'design') ;
#6831=PRODUCT_DEFINITION('Washer_1','Washer_1',#6842,#6827) ;
#6842=PRODUCT_DEFINITION_FORMATION('',$,#6867) ;
#6862=APPLICATION_CONTEXT(
'Core Data for Automotive Mechanical Design Process') ;
#6863=PRODUCT_CONTEXT('part definition',#6862,'mechanical') ;
#6867=PRODUCT('Washer_1','Washer_1',$,(#6863)) ;
#6877=PRESENTATION_STYLE_ASSIGNMENT((#6880)) ;
#6880=SURFACE_STYLE_USAGE(.BOTH.,#6883) ;
#6883=SURFACE_SIDE_STYLE('',(#6886)) ;
#6886=SURFACE_STYLE_FILL_AREA(#6889) ;
#6889=FILL_AREA_STYLE('Opaque(203,203,203)',(#6892)) ;
#6892=FILL_AREA_STYLE_COLOUR('Opaque(203,203,203)',#6895) ;
#6895=COLOUR_RGB('Opaque(203,203,203)', 0.31764706, 0.68627451, 0.89019608) ;
ENDSEC;
END-ISO-10303-21;
